ISO-10303-21;
HEADER;
FILE_DESCRIPTION (('STEP AP214'),
    '1' );
FILE_NAME ('Bushing.step',
    '2026-10-28T16:39:03',
    ( '' ),
    ( '' ),
    'SwSTEP 2.0',
    'SolidWorks 2024',
    '' );
FILE_SCHEMA (( 'AUTOMOTIVE_DESIGN' ));
ENDSEC;

DATA;
#28=VERTEX_POINT ( 'NONE', #2799 ) ;
#33=EDGE_CURVE ( 'NONE', #7631, #7527, #437, .T. ) ;
#40=LINE ( 'NONE', #6225, #5683 ) ;
#49=DIRECTION ( 'NONE',  ( 0.000000000000000000, 0.000000000000000000, 1.000000000000000000 ) ) ;
#50=AXIS2_PLACEMENT_3D ( 'NONE', #3727, #3599, #6048 ) ;
#78=CARTESIAN_POINT ( 'NONE',  ( 1.320471425210250835E-15, 0.000000000000000000, 0.000000000000000000 ) ) ;
#87=SHAPE_DEFINITION_REPRESENTATION ( #2063, #2908 ) ;
#103=VERTEX_POINT ( 'NONE', #2394 ) ;
#111=ORIENTED_EDGE ( 'NONE', *, *, #2037, .T. ) ;
#132=CARTESIAN_POINT ( 'NONE',  ( 125.0000000000000000, 0.000000000000000000, 0.000000000000000000 ) ) ;
#150=VERTEX_POINT ( 'NONE', #4789 ) ;
#248=DIRECTION ( 'NONE',  ( 0.000000000000000000, 0.000000000000000000, -1.000000000000000000 ) ) ;
#258=DIRECTION ( 'NONE',  ( 0.000000000000000000, 0.000000000000000000, 1.000000000000000000 ) ) ;
#274=ADVANCED_FACE ( 'NONE', ( #3795 ), #3515, .T. ) ;
#321=ADVANCED_FACE ( 'NONE', ( #1380 ), #689, .T. ) ;
#369=DIRECTION ( 'NONE',  ( 0.000000000000000000, 0.000000000000000000, 1.000000000000000000 ) ) ;
#379=ORIENTED_EDGE ( 'NONE', *, *, #4066, .F. ) ;
#437=CIRCLE ( 'NONE', #4903, 35.78244274809159720 ) ;
#446=DIRECTION ( 'NONE',  ( 0.000000000000000000, 0.000000000000000000, -1.000000000000000000 ) ) ;
#454=CIRCLE ( 'NONE', #3146, 31.24999999999998579 ) ;
#482=AXIS2_PLACEMENT_3D ( 'NONE', #1216, #6036, #3588 ) ;
#496=VECTOR ( 'NONE', #6062, 1000.000000000000000 ) ;
#547=ORIENTED_EDGE ( 'NONE', *, *, #6445, .T. ) ;
#643=DIRECTION ( 'NONE',  ( -1.000000000000000000, -0.000000000000000000, -0.000000000000000000 ) ) ;
#683=LINE ( 'NONE', #1884, #4208 ) ;
#689=CONICAL_SURFACE ( 'NONE', #1714, 31.78244274809162562, 0.7853981633974447263 ) ;
#709=AXIS2_PLACEMENT_3D ( 'NONE', #7627, #5212, #2824 ) ;
#736=CIRCLE ( 'NONE', #7274, 25.00000000000000000 ) ;
#743=DIRECTION ( 'NONE',  ( 1.000000000000000000, 0.000000000000000000, 0.000000000000000000 ) ) ;
#752=AXIS2_PLACEMENT_3D ( 'NONE', #4614, #4175, #7158 ) ;
#766=CARTESIAN_POINT ( 'NONE',  ( 6.602357126051254174E-16, 0.000000000000000000, 0.000000000000000000 ) ) ;
#773=ORIENTED_EDGE ( 'NONE', *, *, #4377, .T. ) ;
#779=CARTESIAN_POINT ( 'NONE',  ( 6.602357126051254174E-16, 0.000000000000000000, 0.000000000000000000 ) ) ;
#830=DIRECTION ( 'NONE',  ( 0.000000000000000000, 0.000000000000000000, 1.000000000000000000 ) ) ;
#847=CARTESIAN_POINT ( 'NONE',  ( 1.320471425210250835E-15, 0.000000000000000000, 25.00000000000000000 ) ) ;
#913=PRODUCT_DEFINITION_FORMATION_WITH_SPECIFIED_SOURCE ( 'ANY', '', #2848, .NOT_KNOWN. ) ;
#929=DIRECTION ( 'NONE',  ( -1.000000000000000000, -0.000000000000000000, -0.000000000000000000 ) ) ;
#940=ORIENTED_EDGE ( 'NONE', *, *, #4377, .F. ) ;
#942=VECTOR ( 'NONE', #3581, 1000.000000000000114 ) ;
#1029=( LENGTH_UNIT ( ) NAMED_UNIT ( * ) SI_UNIT ( .MILLI., .METRE. ) );
#1033=ORIENTED_EDGE ( 'NONE', *, *, #2037, .F. ) ;
#1039=EDGE_LOOP ( 'NONE', ( #3039, #1762 ) ) ;
#1052=EDGE_CURVE ( 'NONE', #7745, #2331, #454, .T. ) ;
#1182=ORIENTED_EDGE ( 'NONE', *, *, #4981, .F. ) ;
#1204=DIRECTION ( 'NONE',  ( 0.000000000000000000, 0.000000000000000000, 1.000000000000000000 ) ) ;
#1216=CARTESIAN_POINT ( 'NONE',  ( 6.602357126051254174E-16, 0.000000000000000000, 0.000000000000000000 ) ) ;
#1221=CIRCLE ( 'NONE', #6857, 25.00000000000000000 ) ;
#1226=EDGE_CURVE ( 'NONE', #5786, #28, #40, .T. ) ;
#1238=CIRCLE ( 'NONE', #7509, 25.00000000000000000 ) ;
#1265=AXIS2_PLACEMENT_3D ( 'NONE', #7035, #929, #258 ) ;
#1268=DIRECTION ( 'NONE',  ( -1.000000000000000000, -0.000000000000000000, -0.000000000000000000 ) ) ;
#1290=DIRECTION ( 'NONE',  ( -1.000000000000000000, -0.000000000000000000, -0.000000000000000000 ) ) ;
#1315=EDGE_LOOP ( 'NONE', ( #1639, #6362, #7095, #4419 ) ) ;
#1338=CARTESIAN_POINT ( 'NONE',  ( 0.000000000000000000, 0.000000000000000000, 0.000000000000000000 ) ) ;
#1340=VECTOR ( 'NONE', #2847, 1000.000000000000000 ) ;
#1372=CARTESIAN_POINT ( 'NONE',  ( 0.000000000000000000, 0.000000000000000000, 0.000000000000000000 ) ) ;
#1380=FACE_OUTER_BOUND ( 'NONE', #1581, .T. ) ;
#1414=EDGE_LOOP ( 'NONE', ( #5458, #2479, #1627, #1182 ) ) ;
#1440=ADVANCED_FACE ( 'NONE', ( #1864 ), #5483, .F. ) ;
#1447=DIRECTION ( 'NONE',  ( -1.000000000000000000, -0.000000000000000000, -0.000000000000000000 ) ) ;
#1465=VECTOR ( 'NONE', #643, 1000.000000000000000 ) ;
#1543=( LENGTH_UNIT ( ) NAMED_UNIT ( * ) SI_UNIT ( .MILLI., .METRE. ) );
#1581=EDGE_LOOP ( 'NONE', ( #940, #7168, #1751, #4070 ) ) ;
#1613=FACE_OUTER_BOUND ( 'NONE', #1315, .T. ) ;
#1616=ORIENTED_EDGE ( 'NONE', *, *, #33, .F. ) ;
#1627=ORIENTED_EDGE ( 'NONE', *, *, #5908, .T. ) ;
#1639=ORIENTED_EDGE ( 'NONE', *, *, #7090, .T. ) ;
#1655=DIRECTION ( 'NONE',  ( 0.000000000000000000, 0.000000000000000000, 1.000000000000000000 ) ) ;
#1686=ORIENTED_EDGE ( 'NONE', *, *, #6363, .T. ) ;
#1714=AXIS2_PLACEMENT_3D ( 'NONE', #779, #2551, #3232 ) ;
#1718=DIRECTION ( 'NONE',  ( -1.000000000000000000, -0.000000000000000000, -0.000000000000000000 ) ) ;
#1741=EDGE_CURVE ( 'NONE', #6534, #7849, #3015, .T. ) ;
#1743=MANIFOLD_SOLID_BREP ( 'Pah1', #7475 ) ;
#1751=ORIENTED_EDGE ( 'NONE', *, *, #5908, .F. ) ;
#1760=CARTESIAN_POINT ( 'NONE',  ( 0.000000000000000000, 0.000000000000000000, 0.000000000000000000 ) ) ;
#1762=ORIENTED_EDGE ( 'NONE', *, *, #1741, .F. ) ;
#1817=DIRECTION ( 'NONE',  ( 1.000000000000000000, 0.000000000000000000, 0.000000000000000000 ) ) ;
#1835=ORIENTED_EDGE ( 'NONE', *, *, #6158, .T. ) ;
#1842=DIRECTION ( 'NONE',  ( -1.000000000000000000, -0.000000000000000000, -0.000000000000000000 ) ) ;
#1845=AXIS2_PLACEMENT_3D ( 'NONE', #1905, #743, #4380 ) ;
#1864=FACE_OUTER_BOUND ( 'NONE', #5811, .T. ) ;
#1876=EDGE_LOOP ( 'NONE', ( #4967, #6168, #7080, #5452 ) ) ;
#1877=PRODUCT_DEFINITION ( 'UNKNOWN', '', #913, #5431 ) ;
#1884=CARTESIAN_POINT ( 'NONE',  ( 0.000000000000000000, 4.382085397712380109E-15, -35.78244274809159720 ) ) ;
#1895=CYLINDRICAL_SURFACE ( 'NONE', #6216, 25.00000000000000000 ) ;
#1903=FACE_OUTER_BOUND ( 'NONE', #5737, .T. ) ;
#1905=CARTESIAN_POINT ( 'NONE',  ( 6.602357126051254174E-16, 0.000000000000000000, 0.000000000000000000 ) ) ;
#1950=LINE ( 'NONE', #6214, #1465 ) ;
#1994=EDGE_CURVE ( 'NONE', #5786, #4514, #1221, .T. ) ;
#2025=ADVANCED_FACE ( 'NONE', ( #4942 ), #1895, .F. ) ;
#2037=EDGE_CURVE ( 'NONE', #7527, #7631, #2757, .T. ) ;
#2040=ORIENTED_EDGE ( 'NONE', *, *, #4989, .F. ) ;
#2054=ORIENTED_EDGE ( 'NONE', *, *, #7285, .T. ) ;
#2063=PRODUCT_DEFINITION_SHAPE ( 'NONE', 'NONE',  #1877 ) ;
#2069=DIRECTION ( 'NONE',  ( -1.000000000000000000, -0.000000000000000000, -0.000000000000000000 ) ) ;
#2163=CIRCLE ( 'NONE', #6649, 25.00000000000000000 ) ;
#2173=FACE_BOUND ( 'NONE', #3436, .T. ) ;
#2180=EDGE_CURVE ( 'NONE', #4623, #103, #7862, .T. ) ;
#2185=DIRECTION ( 'NONE',  ( -1.000000000000000000, -0.000000000000000000, -0.000000000000000000 ) ) ;
#2218=FACE_OUTER_BOUND ( 'NONE', #1414, .T. ) ;
#2223=CARTESIAN_POINT ( 'NONE',  ( 125.0000000000000000, 3.061616997868383043E-15, -25.00000000000000000 ) ) ;
#2225=( NAMED_UNIT ( * ) PLANE_ANGLE_UNIT ( ) SI_UNIT ( $, .RADIAN. ) );
#2232=ORIENTED_EDGE ( 'NONE', *, *, #4981, .T. ) ;
#2234=( NAMED_UNIT ( * ) SI_UNIT ( $, .STERADIAN. ) SOLID_ANGLE_UNIT ( ) );
#2238=CARTESIAN_POINT ( 'NONE',  ( 12.50000000000000000, 0.000000000000000000, 0.000000000000000000 ) ) ;
#2254=DIRECTION ( 'NONE',  ( 1.000000000000000000, 0.000000000000000000, 0.000000000000000000 ) ) ;
#2278=( NAMED_UNIT ( * ) PLANE_ANGLE_UNIT ( ) SI_UNIT ( $, .RADIAN. ) );
#2287=ORIENTED_EDGE ( 'NONE', *, *, #1994, .F. ) ;
#2296=CYLINDRICAL_SURFACE ( 'NONE', #6979, 31.24999999999999289 ) ;
#2331=VERTEX_POINT ( 'NONE', #2338 ) ;
#2338=CARTESIAN_POINT ( 'NONE',  ( 12.50000000000000000, 3.827021247335477324E-15, -31.24999999999998579 ) ) ;
#2351=DIRECTION ( 'NONE',  ( 1.000000000000000000, 0.000000000000000000, 0.000000000000000000 ) ) ;
#2371=AXIS2_PLACEMENT_3D ( 'NONE', #4537, #4651, #1655 ) ;
#2394=CARTESIAN_POINT ( 'NONE',  ( 4.000000000000004441, 0.000000000000000000, 35.78244274809159720 ) ) ;
#2415=CARTESIAN_POINT ( 'NONE',  ( 1.320471425210250835E-15, 0.000000000000000000, 0.000000000000000000 ) ) ;
#2479=ORIENTED_EDGE ( 'NONE', *, *, #6468, .T. ) ;
#2485=EDGE_CURVE ( 'NONE', #4115, #4623, #5047, .T. ) ;
#2493=DIRECTION ( 'NONE',  ( 1.000000000000000000, 0.000000000000000000, 0.000000000000000000 ) ) ;
#2551=DIRECTION ( 'NONE',  ( 1.000000000000000000, 0.000000000000000000, 0.000000000000000000 ) ) ;
#2657=PLANE ( 'NONE',  #6011 ) ;
#2682=AXIS2_PLACEMENT_3D ( 'NONE', #7348, #2493, #4974 ) ;
#2700=ADVANCED_FACE ( 'NONE', ( #6099 ), #2296, .T. ) ;
#2757=CIRCLE ( 'NONE', #2371, 35.78244274809159720 ) ;
#2773=ADVANCED_FACE ( 'NONE', ( #4125, #3055 ), #6577, .F. ) ;
#2799=CARTESIAN_POINT ( 'NONE',  ( 1.320471425210250835E-15, 3.061616997868383043E-15, -25.00000000000000000 ) ) ;
#2801=PLANE ( 'NONE',  #7025 ) ;
#2811=VECTOR ( 'NONE', #1842, 1000.000000000000000 ) ;
#2824=DIRECTION ( 'NONE',  ( 0.000000000000000000, 0.000000000000000000, 1.000000000000000000 ) ) ;
#2826=CARTESIAN_POINT ( 'NONE',  ( 0.000000000000000000, 0.000000000000000000, 0.000000000000000000 ) ) ;
#2847=DIRECTION ( 'NONE',  ( -1.000000000000000000, -0.000000000000000000, -0.000000000000000000 ) ) ;
#2848=PRODUCT ( 'Bushing', 'Bushing', '', ( #6789 ) ) ;
#2888=EDGE_CURVE ( 'NONE', #4514, #4723, #1950, .T. ) ;
#2908=SHAPE_REPRESENTATION ( 'Bushing', ( #5785 ), #4233 ) ;
#2980=CARTESIAN_POINT ( 'NONE',  ( 0.000000000000000000, 0.000000000000000000, 35.78244274809159720 ) ) ;
#3015=CIRCLE ( 'NONE', #5048, 31.25000000000000000 ) ;
#3039=ORIENTED_EDGE ( 'NONE', *, *, #7090, .F. ) ;
#3055=FACE_BOUND ( 'NONE', #3679, .T. ) ;
#3058=ORIENTED_EDGE ( 'NONE', *, *, #2888, .T. ) ;
#3110=DIRECTION ( 'NONE',  ( 0.000000000000000000, 0.000000000000000000, -1.000000000000000000 ) ) ;
#3125=EDGE_CURVE ( 'NONE', #6534, #2331, #7133, .T. ) ;
#3146=AXIS2_PLACEMENT_3D ( 'NONE', #4768, #5865, #369 ) ;
#3232=DIRECTION ( 'NONE',  ( 0.000000000000000000, 0.000000000000000000, -1.000000000000000000 ) ) ;
#3375=CARTESIAN_POINT ( 'NONE',  ( 125.0000000000000000, 0.000000000000000000, 0.000000000000000000 ) ) ;
#3432=CARTESIAN_POINT ( 'NONE',  ( 125.0000000000000000, 0.000000000000000000, 0.000000000000000000 ) ) ;
#3436=EDGE_LOOP ( 'NONE', ( #7512, #4705 ) ) ;
#3450=CARTESIAN_POINT ( 'NONE',  ( 12.50000000000000000, 4.382085397712380109E-15, -35.78244274809159720 ) ) ;
#3469=ADVANCED_FACE ( 'NONE', ( #2218 ), #5792, .T. ) ;
#3515=CONICAL_SURFACE ( 'NONE', #1845, 31.78244274809162562, 0.7853981633974447263 ) ;
#3575=CIRCLE ( 'NONE', #752, 31.24999999999998579 ) ;
#3581=DIRECTION ( 'NONE',  ( 0.7071067811865500152, 8.659560562354903276E-17, 0.7071067811865451302 ) ) ;
#3588=DIRECTION ( 'NONE',  ( 0.000000000000000000, 0.000000000000000000, -1.000000000000000000 ) ) ;
#3594=ORIENTED_EDGE ( 'NONE', *, *, #1226, .T. ) ;
#3599=DIRECTION ( 'NONE',  ( -1.000000000000000000, -0.000000000000000000, -0.000000000000000000 ) ) ;
#3621=CARTESIAN_POINT ( 'NONE',  ( 6.602357126051254174E-16, 3.892226678053441094E-15, 31.78244274809162562 ) ) ;
#3641=ORIENTED_EDGE ( 'NONE', *, *, #2180, .F. ) ;
#3679=EDGE_LOOP ( 'NONE', ( #6049, #2040 ) ) ;
#3727=CARTESIAN_POINT ( 'NONE',  ( 0.000000000000000000, 0.000000000000000000, 0.000000000000000000 ) ) ;
#3756=ORIENTED_EDGE ( 'NONE', *, *, #2485, .T. ) ;
#3774=ORIENTED_EDGE ( 'NONE', *, *, #1052, .T. ) ;
#3795=FACE_OUTER_BOUND ( 'NONE', #5960, .T. ) ;
#3822=DIRECTION ( 'NONE',  ( -1.000000000000000000, -0.000000000000000000, -0.000000000000000000 ) ) ;
#3888=EDGE_LOOP ( 'NONE', ( #1616, #1033 ) ) ;
#3936=LINE ( 'NONE', #5789, #5102 ) ;
#4016=CYLINDRICAL_SURFACE ( 'NONE', #6266, 31.24999999999999289 ) ;
#4022=DIRECTION ( 'NONE',  ( 0.000000000000000000, 0.000000000000000000, 1.000000000000000000 ) ) ;
#4037=FACE_OUTER_BOUND ( 'NONE', #3888, .T. ) ;
#4066=EDGE_CURVE ( 'NONE', #4514, #5786, #1238, .T. ) ;
#4070=ORIENTED_EDGE ( 'NONE', *, *, #6158, .F. ) ;
#4110=CARTESIAN_POINT ( 'NONE',  ( 0.000000000000000000, 0.000000000000000000, 0.000000000000000000 ) ) ;
#4115=VERTEX_POINT ( 'NONE', #4264 ) ;
#4125=FACE_OUTER_BOUND ( 'NONE', #6993, .T. ) ;
#4175=DIRECTION ( 'NONE',  ( -1.000000000000000000, -0.000000000000000000, -0.000000000000000000 ) ) ;
#4186=DIRECTION ( 'NONE',  ( 0.000000000000000000, 0.000000000000000000, 1.000000000000000000 ) ) ;
#4192=ADVANCED_FACE ( 'NONE', ( #1903 ), #4345, .T. ) ;
#4208=VECTOR ( 'NONE', #4327, 1000.000000000000000 ) ;
#4209=ADVANCED_BREP_SHAPE_REPRESENTATION ( '', ( #1743, #5785 ), #4233 ) ;
#4233=( GEOMETRIC_REPRESENTATION_CONTEXT ( 3 ) GLOBAL_UNCERTAINTY_ASSIGNED_CONTEXT ( ( #5841 ) ) GLOBAL_UNIT_ASSIGNED_CONTEXT ( ( #1029, #2278, #2234 ) ) REPRESENTATION_CONTEXT ( 'NONE', 'WORKASPACE' ) );
#4238=CARTESIAN_POINT ( 'NONE',  ( 12.50000000000000000, 0.000000000000000000, 35.78244274809159720 ) ) ;
#4264=CARTESIAN_POINT ( 'NONE',  ( 6.602357126051254174E-16, 0.000000000000000000, -31.78244274809162562 ) ) ;
#4273=AXIS2_PLACEMENT_3D ( 'NONE', #766, #6265, #248 ) ;
#4288=EDGE_LOOP ( 'NONE', ( #3774, #2054 ) ) ;
#4291=LINE ( 'NONE', #4854, #2811 ) ;
#4327=DIRECTION ( 'NONE',  ( -1.000000000000000000, -0.000000000000000000, -0.000000000000000000 ) ) ;
#4340=DIRECTION ( 'NONE',  ( 0.000000000000000000, 0.000000000000000000, 1.000000000000000000 ) ) ;
#4345=CYLINDRICAL_SURFACE ( 'NONE', #4953, 35.78244274809159720 ) ;
#4377=EDGE_CURVE ( 'NONE', #4623, #4115, #4432, .T. ) ;
#4380=DIRECTION ( 'NONE',  ( 0.000000000000000000, 0.000000000000000000, -1.000000000000000000 ) ) ;
#4419=ORIENTED_EDGE ( 'NONE', *, *, #6379, .F. ) ;
#4420=DIRECTION ( 'NONE',  ( -1.000000000000000000, -0.000000000000000000, -0.000000000000000000 ) ) ;
#4432=CIRCLE ( 'NONE', #482, 31.78244274809162562 ) ;
#4452=DIRECTION ( 'NONE',  ( -0.000000000000000000, 0.000000000000000000, 1.000000000000000000 ) ) ;
#4514=VERTEX_POINT ( 'NONE', #7507 ) ;
#4534=CARTESIAN_POINT ( 'NONE',  ( 6.602357126051254174E-16, 4.137156037882910601E-15, 31.78244274809162562 ) ) ;
#4537=CARTESIAN_POINT ( 'NONE',  ( 12.50000000000000000, 0.000000000000000000, 0.000000000000000000 ) ) ;
#4589=AXIS2_PLACEMENT_3D ( 'NONE', #4985, #1817, #3110 ) ;
#4614=CARTESIAN_POINT ( 'NONE',  ( 12.50000000000000000, 0.000000000000000000, 0.000000000000000000 ) ) ;
#4623=VERTEX_POINT ( 'NONE', #4534 ) ;
#4651=DIRECTION ( 'NONE',  ( -1.000000000000000000, -0.000000000000000000, -0.000000000000000000 ) ) ;
#4705=ORIENTED_EDGE ( 'NONE', *, *, #1994, .T. ) ;
#4723=VERTEX_POINT ( 'NONE', #847 ) ;
#4768=CARTESIAN_POINT ( 'NONE',  ( 12.50000000000000000, 0.000000000000000000, 0.000000000000000000 ) ) ;
#4789=CARTESIAN_POINT ( 'NONE',  ( 4.000000000000004441, 4.382085397712380109E-15, -35.78244274809159720 ) ) ;
#4854=CARTESIAN_POINT ( 'NONE',  ( 0.000000000000000000, 0.000000000000000000, 31.24999999999999289 ) ) ;
#4887=DIRECTION ( 'NONE',  ( 0.000000000000000000, 0.000000000000000000, 1.000000000000000000 ) ) ;
#4903=AXIS2_PLACEMENT_3D ( 'NONE', #2238, #2069, #830 ) ;
#4942=FACE_OUTER_BOUND ( 'NONE', #6025, .T. ) ;
#4953=AXIS2_PLACEMENT_3D ( 'NONE', #1338, #4420, #6801 ) ;
#4967=ORIENTED_EDGE ( 'NONE', *, *, #3125, .F. ) ;
#4974=DIRECTION ( 'NONE',  ( 0.000000000000000000, 0.000000000000000000, -1.000000000000000000 ) ) ;
#4981=EDGE_CURVE ( 'NONE', #7631, #103, #7267, .T. ) ;
#4985=CARTESIAN_POINT ( 'NONE',  ( 4.000000000000004441, 0.000000000000000000, 0.000000000000000000 ) ) ;
#4989=EDGE_CURVE ( 'NONE', #28, #4723, #736, .T. ) ;
#5047=CIRCLE ( 'NONE', #4273, 31.78244274809162562 ) ;
#5048=AXIS2_PLACEMENT_3D ( 'NONE', #3432, #2185, #4022 ) ;
#5102=VECTOR ( 'NONE', #6384, 1000.000000000000114 ) ;
#5155=ORIENTED_EDGE ( 'NONE', *, *, #1226, .F. ) ;
#5212=DIRECTION ( 'NONE',  ( -1.000000000000000000, -0.000000000000000000, -0.000000000000000000 ) ) ;
#5230=CIRCLE ( 'NONE', #2682, 35.78244274809159720 ) ;
#5232=CARTESIAN_POINT ( 'NONE',  ( 125.0000000000000000, 0.000000000000000000, 31.25000000000000000 ) ) ;
#5238=FACE_BOUND ( 'NONE', #4288, .T. ) ;
#5260=DIRECTION ( 'NONE',  ( -1.000000000000000000, -0.000000000000000000, -0.000000000000000000 ) ) ;
#5361=DIRECTION ( 'NONE',  ( 0.000000000000000000, 0.000000000000000000, 1.000000000000000000 ) ) ;
#5431=PRODUCT_DEFINITION_CONTEXT ( 'detailed design', #6650, 'design' ) ;
#5452=ORIENTED_EDGE ( 'NONE', *, *, #7285, .F. ) ;
#5458=ORIENTED_EDGE ( 'NONE', *, *, #33, .T. ) ;
#5483=CYLINDRICAL_SURFACE ( 'NONE', #50, 25.00000000000000000 ) ;
#5683=VECTOR ( 'NONE', #1290, 1000.000000000000000 ) ;
#5700=CARTESIAN_POINT ( 'NONE',  ( 125.0000000000000000, 3.827021247335478902E-15, -31.25000000000000000 ) ) ;
#5737=EDGE_LOOP ( 'NONE', ( #7812, #111, #2232, #1686 ) ) ;
#5765=UNCERTAINTY_MEASURE_WITH_UNIT (LENGTH_MEASURE( 1.000000000000000082E-05 ), #1543, 'distance_accuracy_value', 'NONE');
#5785=AXIS2_PLACEMENT_3D ( 'NONE', #4110, #4186, #2351 ) ;
#5786=VERTEX_POINT ( 'NONE', #2223 ) ;
#5789=CARTESIAN_POINT ( 'NONE',  ( 6.602357126051254174E-16, 0.000000000000000000, -31.78244274809162562 ) ) ;
#5792=CYLINDRICAL_SURFACE ( 'NONE', #709, 35.78244274809159720 ) ;
#5811=EDGE_LOOP ( 'NONE', ( #5155, #379, #3058, #547 ) ) ;
#5832=DIRECTION ( 'NONE',  ( 0.000000000000000000, 0.000000000000000000, 1.000000000000000000 ) ) ;
#5841=UNCERTAINTY_MEASURE_WITH_UNIT (LENGTH_MEASURE( 1.000000000000000082E-05 ), #1029, 'distance_accuracy_value', 'NONE');
#5865=DIRECTION ( 'NONE',  ( -1.000000000000000000, -0.000000000000000000, -0.000000000000000000 ) ) ;
#5908=EDGE_CURVE ( 'NONE', #150, #103, #6777, .T. ) ;
#5960=EDGE_LOOP ( 'NONE', ( #3641, #6808, #1835, #6126 ) ) ;
#6011=AXIS2_PLACEMENT_3D ( 'NONE', #3375, #6426, #4452 ) ;
#6025=EDGE_LOOP ( 'NONE', ( #2287, #3594, #7823, #6960 ) ) ;
#6036=DIRECTION ( 'NONE',  ( -1.000000000000000000, -0.000000000000000000, -0.000000000000000000 ) ) ;
#6048=DIRECTION ( 'NONE',  ( 0.000000000000000000, 0.000000000000000000, 1.000000000000000000 ) ) ;
#6049=ORIENTED_EDGE ( 'NONE', *, *, #6445, .F. ) ;
#6062=DIRECTION ( 'NONE',  ( -1.000000000000000000, -0.000000000000000000, -0.000000000000000000 ) ) ;
#6066=ADVANCED_FACE ( 'NONE', ( #7623, #2173 ), #2657, .F. ) ;
#6085=STYLED_ITEM('',(#7976),#1743);
#6093=CARTESIAN_POINT ( 'NONE',  ( 12.50000000000000000, 0.000000000000000000, 31.24999999999998579 ) ) ;
#6099=FACE_OUTER_BOUND ( 'NONE', #1876, .T. ) ;
#6103=DIRECTION ( 'NONE',  ( -1.000000000000000000, -0.000000000000000000, -0.000000000000000000 ) ) ;
#6126=ORIENTED_EDGE ( 'NONE', *, *, #6363, .F. ) ;
#6158=EDGE_CURVE ( 'NONE', #4115, #150, #3936, .T. ) ;
#6168=ORIENTED_EDGE ( 'NONE', *, *, #1741, .T. ) ;
#6182=APPLICATION_CONTEXT ( 'automotive_design' ) ;
#6214=CARTESIAN_POINT ( 'NONE',  ( 0.000000000000000000, 0.000000000000000000, 25.00000000000000000 ) ) ;
#6216=AXIS2_PLACEMENT_3D ( 'NONE', #1372, #3822, #4340 ) ;
#6225=CARTESIAN_POINT ( 'NONE',  ( 0.000000000000000000, 3.061616997868383043E-15, -25.00000000000000000 ) ) ;
#6265=DIRECTION ( 'NONE',  ( -1.000000000000000000, -0.000000000000000000, -0.000000000000000000 ) ) ;
#6266=AXIS2_PLACEMENT_3D ( 'NONE', #2826, #5260, #5832 ) ;
#6362=ORIENTED_EDGE ( 'NONE', *, *, #3125, .T. ) ;
#6363=EDGE_CURVE ( 'NONE', #103, #150, #5230, .T. ) ;
#6379=EDGE_CURVE ( 'NONE', #7849, #7745, #4291, .T. ) ;
#6384=DIRECTION ( 'NONE',  ( 0.7071067811865500152, 0.000000000000000000, -0.7071067811865451302 ) ) ;
#6426=DIRECTION ( 'NONE',  ( -1.000000000000000000, 0.000000000000000000, -0.000000000000000000 ) ) ;
#6442=DIRECTION ( 'NONE',  ( -1.000000000000000000, 0.000000000000000000, -0.000000000000000000 ) ) ;
#6445=EDGE_CURVE ( 'NONE', #4723, #28, #2163, .T. ) ;
#6468=EDGE_CURVE ( 'NONE', #7527, #150, #683, .T. ) ;
#6524=( NAMED_UNIT ( * ) SI_UNIT ( $, .STERADIAN. ) SOLID_ANGLE_UNIT ( ) );
#6534=VERTEX_POINT ( 'NONE', #5700 ) ;
#6543=DIRECTION ( 'NONE',  ( 0.000000000000000000, 0.000000000000000000, 1.000000000000000000 ) ) ;
#6577=PLANE ( 'NONE',  #7872 ) ;
#6649=AXIS2_PLACEMENT_3D ( 'NONE', #2415, #6701, #1204 ) ;
#6650=APPLICATION_CONTEXT ( 'automotive_design' ) ;
#6701=DIRECTION ( 'NONE',  ( -1.000000000000000000, -0.000000000000000000, -0.000000000000000000 ) ) ;
#6761=CARTESIAN_POINT ( 'NONE',  ( 125.0000000000000000, 0.000000000000000000, 0.000000000000000000 ) ) ;
#6777=CIRCLE ( 'NONE', #4589, 35.78244274809159720 ) ;
#6789=PRODUCT_CONTEXT ( 'NONE', #6182, 'mechanical' ) ;
#6801=DIRECTION ( 'NONE',  ( 0.000000000000000000, 0.000000000000000000, 1.000000000000000000 ) ) ;
#6808=ORIENTED_EDGE ( 'NONE', *, *, #2485, .F. ) ;
#6857=AXIS2_PLACEMENT_3D ( 'NONE', #132, #1447, #49 ) ;
#6960=ORIENTED_EDGE ( 'NONE', *, *, #2888, .F. ) ;
#6979=AXIS2_PLACEMENT_3D ( 'NONE', #1760, #1718, #6543 ) ;
#6993=EDGE_LOOP ( 'NONE', ( #3756, #773 ) ) ;
#7002=ADVANCED_FACE ( 'NONE', ( #4037, #5238 ), #2801, .F. ) ;
#7025=AXIS2_PLACEMENT_3D ( 'NONE', #7772, #6442, #7645 ) ;
#7035=CARTESIAN_POINT ( 'NONE',  ( 125.0000000000000000, 0.000000000000000000, 0.000000000000000000 ) ) ;
#7080=ORIENTED_EDGE ( 'NONE', *, *, #6379, .T. ) ;
#7090=EDGE_CURVE ( 'NONE', #7849, #6534, #7798, .T. ) ;
#7095=ORIENTED_EDGE ( 'NONE', *, *, #1052, .F. ) ;
#7107=MECHANICAL_DESIGN_GEOMETRIC_PRESENTATION_REPRESENTATION('',(#6085),#7245);
#7127=SHAPE_REPRESENTATION_RELATIONSHIP ( 'NONE' , 'NONE' ,  #2908, #4209 ) ;
#7133=LINE ( 'NONE', #7774, #1340 ) ;
#7158=DIRECTION ( 'NONE',  ( 0.000000000000000000, 0.000000000000000000, 1.000000000000000000 ) ) ;
#7168=ORIENTED_EDGE ( 'NONE', *, *, #2180, .T. ) ;
#7216=ADVANCED_FACE ( 'NONE', ( #1613 ), #4016, .T. ) ;
#7245=( GEOMETRIC_REPRESENTATION_CONTEXT ( 3 ) GLOBAL_UNCERTAINTY_ASSIGNED_CONTEXT ( ( #5765 ) ) GLOBAL_UNIT_ASSIGNED_CONTEXT ( ( #1543, #2225, #6524 ) ) REPRESENTATION_CONTEXT ( 'NONE', 'WORKASPACE' ) );
#7267=LINE ( 'NONE', #2980, #496 ) ;
#7274=AXIS2_PLACEMENT_3D ( 'NONE', #78, #6103, #4887 ) ;
#7285=EDGE_CURVE ( 'NONE', #2331, #7745, #3575, .T. ) ;
#7348=CARTESIAN_POINT ( 'NONE',  ( 4.000000000000004441, 0.000000000000000000, 0.000000000000000000 ) ) ;
#7475=CLOSED_SHELL ( 'NONE', ( #321, #7216, #2025, #3469, #4192, #2773, #1440, #6066, #2700, #7002, #274 ) ) ;
#7507=CARTESIAN_POINT ( 'NONE',  ( 125.0000000000000000, 0.000000000000000000, 25.00000000000000000 ) ) ;
#7509=AXIS2_PLACEMENT_3D ( 'NONE', #6761, #1268, #5361 ) ;
#7512=ORIENTED_EDGE ( 'NONE', *, *, #4066, .T. ) ;
#7527=VERTEX_POINT ( 'NONE', #3450 ) ;
#7623=FACE_OUTER_BOUND ( 'NONE', #1039, .T. ) ;
#7627=CARTESIAN_POINT ( 'NONE',  ( 0.000000000000000000, 0.000000000000000000, 0.000000000000000000 ) ) ;
#7631=VERTEX_POINT ( 'NONE', #4238 ) ;
#7645=DIRECTION ( 'NONE',  ( -0.000000000000000000, 0.000000000000000000, 1.000000000000000000 ) ) ;
#7741=CARTESIAN_POINT ( 'NONE',  ( 6.602357126051254174E-16, 5.366506855898817567E-31, 0.000000000000000000 ) ) ;
#7745=VERTEX_POINT ( 'NONE', #6093 ) ;
#7772=CARTESIAN_POINT ( 'NONE',  ( 12.50000000000000000, 0.000000000000000000, 0.000000000000000000 ) ) ;
#7774=CARTESIAN_POINT ( 'NONE',  ( 0.000000000000000000, 3.827021247335478113E-15, -31.24999999999999289 ) ) ;
#7798=CIRCLE ( 'NONE', #1265, 31.25000000000000000 ) ;
#7812=ORIENTED_EDGE ( 'NONE', *, *, #6468, .F. ) ;
#7823=ORIENTED_EDGE ( 'NONE', *, *, #4989, .T. ) ;
#7849=VERTEX_POINT ( 'NONE', #5232 ) ;
#7862=LINE ( 'NONE', #3621, #942 ) ;
#7872=AXIS2_PLACEMENT_3D ( 'NONE', #7741, #2254, #446 ) ;
#7970=COLOUR_RGB('Off White',0.89,0.88,0.83);
#7971=FILL_AREA_STYLE_COLOUR('',#7970);
#7972=FILL_AREA_STYLE('',(#7971));
#7973=SURFACE_STYLE_FILL_AREA(#7972);
#7974=SURFACE_SIDE_STYLE('',(#7973));
#7975=SURFACE_STYLE_USAGE(.BOTH.,#7974);
#7976=PRESENTATION_STYLE_ASSIGNMENT((#7975));
ENDSEC;
END-ISO-10303-21;
